ISO-10303-21;
HEADER;
/* Generated by software containing ST-Developer
 * from STEP Tools, Inc. (www.steptools.com) 
 */

FILE_DESCRIPTION(
/* description */ ('Spur gear reduction stage 2-1 on bearing plates'),
/* implementation_level */ '2;1');

FILE_NAME(
/* name */ 'Cap Screw - M5x20.step',
/* time_stamp */ '2026-10-28T03:22:07-07:00',
/* author */ (''),
/* organization */ (''),
/* preprocessor_version */ 'ST-DEVELOPER v20.2',
/* originating_system */ 'Autodesk Translation Framework v15.17.0.0',
/* authorisation */ '');

FILE_SCHEMA (('AUTOMOTIVE_DESIGN { 1 0 10303 214 3 1 1 }'));
ENDSEC;

DATA;
#10=MECHANICAL_DESIGN_GEOMETRIC_PRESENTATION_REPRESENTATION('',(#958),#53909);
#829=ORIENTED_CLOSED_SHELL('',*,#11283,.F.);
#832=CONICAL_SURFACE('',#12104,0.4,0.785398163397448);
#833=CONICAL_SURFACE('',#12108,0.41,0.785398163397448);
#834=CONICAL_SURFACE('',#12112,0.26,0.463647609000806);
#835=CONICAL_SURFACE('',#12116,0.225,0.785398163397448);
#858=BREP_WITH_VOIDS('Body1',#11282,(#829));
#872=SHAPE_REPRESENTATION_RELATIONSHIP('SRR','None',#54099,#915);
#915=ADVANCED_BREP_SHAPE_REPRESENTATION('',(#858),#53873);
#958=STYLED_ITEM('',(#54404),#858);
#1176=FACE_BOUND('',#2402,.T.);
#1292=PLANE('',#12102);
#1293=PLANE('',#12110);
#1294=PLANE('',#12118);
#1295=PLANE('',#12119);
#1296=PLANE('',#12120);
#1297=PLANE('',#12121);
#1298=PLANE('',#12122);
#1299=PLANE('',#12123);
#1300=PLANE('',#12124);
#1301=PLANE('',#12125);
#1302=PLANE('',#12126);
#1633=FACE_OUTER_BOUND('',#2397,.T.);
#1634=FACE_OUTER_BOUND('',#2398,.T.);
#1635=FACE_OUTER_BOUND('',#2399,.T.);
#1636=FACE_OUTER_BOUND('',#2400,.T.);
#1637=FACE_OUTER_BOUND('',#2401,.T.);
#1638=FACE_OUTER_BOUND('',#2403,.T.);
#1639=FACE_OUTER_BOUND('',#2404,.T.);
#1640=FACE_OUTER_BOUND('',#2405,.T.);
#1641=FACE_OUTER_BOUND('',#2406,.T.);
#1642=FACE_OUTER_BOUND('',#2407,.T.);
#1643=FACE_OUTER_BOUND('',#2408,.T.);
#1644=FACE_OUTER_BOUND('',#2409,.T.);
#1645=FACE_OUTER_BOUND('',#2410,.T.);
#1646=FACE_OUTER_BOUND('',#2411,.T.);
#1647=FACE_OUTER_BOUND('',#2412,.T.);
#1648=FACE_OUTER_BOUND('',#2413,.T.);
#1649=FACE_OUTER_BOUND('',#2414,.T.);
#2397=EDGE_LOOP('',(#7880));
#2398=EDGE_LOOP('',(#7881,#7882,#7883,#7884));
#2399=EDGE_LOOP('',(#7885,#7886,#7887,#7888));
#2400=EDGE_LOOP('',(#7889,#7890,#7891,#7892));
#2401=EDGE_LOOP('',(#7893));
#2402=EDGE_LOOP('',(#7894));
#2403=EDGE_LOOP('',(#7895,#7896,#7897,#7898));
#2404=EDGE_LOOP('',(#7899,#7900,#7901,#7902));
#2405=EDGE_LOOP('',(#7903,#7904,#7905,#7906));
#2406=EDGE_LOOP('',(#7907));
#2407=EDGE_LOOP('',(#7908,#7909,#7910,#7911));
#2408=EDGE_LOOP('',(#7912,#7913,#7914,#7915));
#2409=EDGE_LOOP('',(#7916,#7917,#7918,#7919));
#2410=EDGE_LOOP('',(#7920,#7921,#7922,#7923));
#2411=EDGE_LOOP('',(#7924,#7925,#7926,#7927));
#2412=EDGE_LOOP('',(#7928,#7929,#7930,#7931));
#2413=EDGE_LOOP('',(#7932,#7933,#7934,#7935,#7936,#7937));
#2414=EDGE_LOOP('',(#7938,#7939,#7940,#7941,#7942,#7943));
#3089=LINE('',#16565,#3730);
#3090=LINE('',#16569,#3731);
#3091=LINE('',#16573,#3732);
#3092=LINE('',#16580,#3733);
#3093=LINE('',#16584,#3734);
#3094=LINE('',#16588,#3735);
#3095=LINE('',#16593,#3736);
#3096=LINE('',#16595,#3737);
#3097=LINE('',#16597,#3738);
#3098=LINE('',#16598,#3739);
#3099=LINE('',#16601,#3740);
#3100=LINE('',#16603,#3741);
#3101=LINE('',#16604,#3742);
#3102=LINE('',#16607,#3743);
#3103=LINE('',#16609,#3744);
#3104=LINE('',#16610,#3745);
#3105=LINE('',#16613,#3746);
#3106=LINE('',#16615,#3747);
#3107=LINE('',#16616,#3748);
#3108=LINE('',#16619,#3749);
#3109=LINE('',#16621,#3750);
#3110=LINE('',#16622,#3751);
#3111=LINE('',#16624,#3752);
#3112=LINE('',#16625,#3753);
#3730=VECTOR('',#13694,0.4);
#3731=VECTOR('',#13699,0.425);
#3732=VECTOR('',#13704,0.41);
#3733=VECTOR('',#13713,0.26);
#3734=VECTOR('',#13718,0.25);
#3735=VECTOR('',#13723,0.225);
#3736=VECTOR('',#13728,1.);
#3737=VECTOR('',#13729,1.);
#3738=VECTOR('',#13730,1.);
#3739=VECTOR('',#13731,1.);
#3740=VECTOR('',#13734,1.);
#3741=VECTOR('',#13735,1.);
#3742=VECTOR('',#13736,1.);
#3743=VECTOR('',#13739,1.);
#3744=VECTOR('',#13740,1.);
#3745=VECTOR('',#13741,1.);
#3746=VECTOR('',#13744,1.);
#3747=VECTOR('',#13745,1.);
#3748=VECTOR('',#13746,1.);
#3749=VECTOR('',#13749,1.);
#3750=VECTOR('',#13750,1.);
#3751=VECTOR('',#13751,1.);
#3752=VECTOR('',#13754,1.);
#3753=VECTOR('',#13755,1.);
#4411=CIRCLE('',#12103,0.375);
#4412=CIRCLE('',#12105,0.425);
#4413=CIRCLE('',#12107,0.425);
#4414=CIRCLE('',#12109,0.395);
#4415=CIRCLE('',#12111,0.27);
#4416=CIRCLE('',#12113,0.24505);
#4417=CIRCLE('',#12115,0.24505);
#4418=CIRCLE('',#12117,0.2);
#4960=VERTEX_POINT('',#16560);
#4961=VERTEX_POINT('',#16563);
#4962=VERTEX_POINT('',#16567);
#4963=VERTEX_POINT('',#16571);
#4964=VERTEX_POINT('',#16575);
#4965=VERTEX_POINT('',#16578);
#4966=VERTEX_POINT('',#16582);
#4967=VERTEX_POINT('',#16586);
#4968=VERTEX_POINT('',#16591);
#4969=VERTEX_POINT('',#16592);
#4970=VERTEX_POINT('',#16594);
#4971=VERTEX_POINT('',#16596);
#4972=VERTEX_POINT('',#16600);
#4973=VERTEX_POINT('',#16602);
#4974=VERTEX_POINT('',#16606);
#4975=VERTEX_POINT('',#16608);
#4976=VERTEX_POINT('',#16612);
#4977=VERTEX_POINT('',#16614);
#4978=VERTEX_POINT('',#16618);
#4979=VERTEX_POINT('',#16620);
#6082=EDGE_CURVE('',#4960,#4960,#4411,.T.);
#6083=EDGE_CURVE('',#4961,#4961,#4412,.T.);
#6084=EDGE_CURVE('',#4961,#4960,#3089,.T.);
#6085=EDGE_CURVE('',#4962,#4962,#4413,.T.);
#6086=EDGE_CURVE('',#4962,#4961,#3090,.T.);
#6087=EDGE_CURVE('',#4963,#4963,#4414,.T.);
#6088=EDGE_CURVE('',#4963,#4962,#3091,.T.);
#6089=EDGE_CURVE('',#4964,#4964,#4415,.T.);
#6090=EDGE_CURVE('',#4965,#4965,#4416,.F.);
#6091=EDGE_CURVE('',#4965,#4964,#3092,.T.);
#6092=EDGE_CURVE('',#4966,#4966,#4417,.F.);
#6093=EDGE_CURVE('',#4966,#4965,#3093,.T.);
#6094=EDGE_CURVE('',#4967,#4967,#4418,.T.);
#6095=EDGE_CURVE('',#4967,#4966,#3094,.T.);
#6096=EDGE_CURVE('',#4968,#4969,#3095,.T.);
#6097=EDGE_CURVE('',#4969,#4970,#3096,.T.);
#6098=EDGE_CURVE('',#4970,#4971,#3097,.T.);
#6099=EDGE_CURVE('',#4968,#4971,#3098,.T.);
#6100=EDGE_CURVE('',#4969,#4972,#3099,.T.);
#6101=EDGE_CURVE('',#4972,#4973,#3100,.T.);
#6102=EDGE_CURVE('',#4973,#4970,#3101,.T.);
#6103=EDGE_CURVE('',#4972,#4974,#3102,.T.);
#6104=EDGE_CURVE('',#4974,#4975,#3103,.T.);
#6105=EDGE_CURVE('',#4975,#4973,#3104,.T.);
#6106=EDGE_CURVE('',#4974,#4976,#3105,.T.);
#6107=EDGE_CURVE('',#4976,#4977,#3106,.T.);
#6108=EDGE_CURVE('',#4977,#4975,#3107,.T.);
#6109=EDGE_CURVE('',#4976,#4978,#3108,.T.);
#6110=EDGE_CURVE('',#4978,#4979,#3109,.T.);
#6111=EDGE_CURVE('',#4979,#4977,#3110,.T.);
#6112=EDGE_CURVE('',#4978,#4968,#3111,.T.);
#6113=EDGE_CURVE('',#4971,#4979,#3112,.T.);
#7880=ORIENTED_EDGE('',*,*,#6082,.F.);
#7881=ORIENTED_EDGE('',*,*,#6083,.F.);
#7882=ORIENTED_EDGE('',*,*,#6084,.T.);
#7883=ORIENTED_EDGE('',*,*,#6082,.T.);
#7884=ORIENTED_EDGE('',*,*,#6084,.F.);
#7885=ORIENTED_EDGE('',*,*,#6085,.F.);
#7886=ORIENTED_EDGE('',*,*,#6086,.T.);
#7887=ORIENTED_EDGE('',*,*,#6083,.T.);
#7888=ORIENTED_EDGE('',*,*,#6086,.F.);
#7889=ORIENTED_EDGE('',*,*,#6087,.F.);
#7890=ORIENTED_EDGE('',*,*,#6088,.T.);
#7891=ORIENTED_EDGE('',*,*,#6085,.T.);
#7892=ORIENTED_EDGE('',*,*,#6088,.F.);
#7893=ORIENTED_EDGE('',*,*,#6087,.T.);
#7894=ORIENTED_EDGE('',*,*,#6089,.F.);
#7895=ORIENTED_EDGE('',*,*,#6090,.F.);
#7896=ORIENTED_EDGE('',*,*,#6091,.T.);
#7897=ORIENTED_EDGE('',*,*,#6089,.T.);
#7898=ORIENTED_EDGE('',*,*,#6091,.F.);
#7899=ORIENTED_EDGE('',*,*,#6092,.F.);
#7900=ORIENTED_EDGE('',*,*,#6093,.T.);
#7901=ORIENTED_EDGE('',*,*,#6090,.T.);
#7902=ORIENTED_EDGE('',*,*,#6093,.F.);
#7903=ORIENTED_EDGE('',*,*,#6094,.F.);
#7904=ORIENTED_EDGE('',*,*,#6095,.T.);
#7905=ORIENTED_EDGE('',*,*,#6092,.T.);
#7906=ORIENTED_EDGE('',*,*,#6095,.F.);
#7907=ORIENTED_EDGE('',*,*,#6094,.T.);
#7908=ORIENTED_EDGE('',*,*,#6096,.T.);
#7909=ORIENTED_EDGE('',*,*,#6097,.T.);
#7910=ORIENTED_EDGE('',*,*,#6098,.T.);
#7911=ORIENTED_EDGE('',*,*,#6099,.F.);
#7912=ORIENTED_EDGE('',*,*,#6100,.T.);
#7913=ORIENTED_EDGE('',*,*,#6101,.T.);
#7914=ORIENTED_EDGE('',*,*,#6102,.T.);
#7915=ORIENTED_EDGE('',*,*,#6097,.F.);
#7916=ORIENTED_EDGE('',*,*,#6103,.T.);
#7917=ORIENTED_EDGE('',*,*,#6104,.T.);
#7918=ORIENTED_EDGE('',*,*,#6105,.T.);
#7919=ORIENTED_EDGE('',*,*,#6101,.F.);
#7920=ORIENTED_EDGE('',*,*,#6106,.T.);
#7921=ORIENTED_EDGE('',*,*,#6107,.T.);
#7922=ORIENTED_EDGE('',*,*,#6108,.T.);
#7923=ORIENTED_EDGE('',*,*,#6104,.F.);
#7924=ORIENTED_EDGE('',*,*,#6109,.T.);
#7925=ORIENTED_EDGE('',*,*,#6110,.T.);
#7926=ORIENTED_EDGE('',*,*,#6111,.T.);
#7927=ORIENTED_EDGE('',*,*,#6107,.F.);
#7928=ORIENTED_EDGE('',*,*,#6112,.T.);
#7929=ORIENTED_EDGE('',*,*,#6099,.T.);
#7930=ORIENTED_EDGE('',*,*,#6113,.T.);
#7931=ORIENTED_EDGE('',*,*,#6110,.F.);
#7932=ORIENTED_EDGE('',*,*,#6112,.F.);
#7933=ORIENTED_EDGE('',*,*,#6109,.F.);
#7934=ORIENTED_EDGE('',*,*,#6106,.F.);
#7935=ORIENTED_EDGE('',*,*,#6103,.F.);
#7936=ORIENTED_EDGE('',*,*,#6100,.F.);
#7937=ORIENTED_EDGE('',*,*,#6096,.F.);
#7938=ORIENTED_EDGE('',*,*,#6113,.F.);
#7939=ORIENTED_EDGE('',*,*,#6098,.F.);
#7940=ORIENTED_EDGE('',*,*,#6102,.F.);
#7941=ORIENTED_EDGE('',*,*,#6105,.F.);
#7942=ORIENTED_EDGE('',*,*,#6108,.F.);
#7943=ORIENTED_EDGE('',*,*,#6111,.F.);
#10496=CYLINDRICAL_SURFACE('',#12106,0.425);
#10497=CYLINDRICAL_SURFACE('',#12114,0.24505);
#10753=ADVANCED_FACE('',(#1633),#1292,.T.);
#10754=ADVANCED_FACE('',(#1634),#832,.T.);
#10755=ADVANCED_FACE('',(#1635),#10496,.T.);
#10756=ADVANCED_FACE('',(#1636),#833,.T.);
#10757=ADVANCED_FACE('',(#1637,#1176),#1293,.T.);
#10758=ADVANCED_FACE('',(#1638),#834,.T.);
#10759=ADVANCED_FACE('',(#1639),#10497,.T.);
#10760=ADVANCED_FACE('',(#1640),#835,.T.);
#10761=ADVANCED_FACE('',(#1641),#1294,.T.);
#10762=ADVANCED_FACE('',(#1642),#1295,.F.);
#10763=ADVANCED_FACE('',(#1643),#1296,.F.);
#10764=ADVANCED_FACE('',(#1644),#1297,.F.);
#10765=ADVANCED_FACE('',(#1645),#1298,.F.);
#10766=ADVANCED_FACE('',(#1646),#1299,.F.);
#10767=ADVANCED_FACE('',(#1647),#1300,.F.);
#10768=ADVANCED_FACE('',(#1648),#1301,.F.);
#10769=ADVANCED_FACE('',(#1649),#1302,.F.);
#11282=CLOSED_SHELL('',(#10753,#10754,#10755,#10756,#10757,#10758,#10759,
#10760,#10761));
#11283=CLOSED_SHELL('',(#10762,#10763,#10764,#10765,#10766,#10767,#10768,
#10769));
#12101=AXIS2_PLACEMENT_3D('',#16558,#13684,#13685);
#12102=AXIS2_PLACEMENT_3D('',#16559,#13686,#13687);
#12103=AXIS2_PLACEMENT_3D('',#16561,#13688,#13689);
#12104=AXIS2_PLACEMENT_3D('',#16562,#13690,#13691);
#12105=AXIS2_PLACEMENT_3D('',#16564,#13692,#13693);
#12106=AXIS2_PLACEMENT_3D('',#16566,#13695,#13696);
#12107=AXIS2_PLACEMENT_3D('',#16568,#13697,#13698);
#12108=AXIS2_PLACEMENT_3D('',#16570,#13700,#13701);
#12109=AXIS2_PLACEMENT_3D('',#16572,#13702,#13703);
#12110=AXIS2_PLACEMENT_3D('',#16574,#13705,#13706);
#12111=AXIS2_PLACEMENT_3D('',#16576,#13707,#13708);
#12112=AXIS2_PLACEMENT_3D('',#16577,#13709,#13710);
#12113=AXIS2_PLACEMENT_3D('',#16579,#13711,#13712);
#12114=AXIS2_PLACEMENT_3D('',#16581,#13714,#13715);
#12115=AXIS2_PLACEMENT_3D('',#16583,#13716,#13717);
#12116=AXIS2_PLACEMENT_3D('',#16585,#13719,#13720);
#12117=AXIS2_PLACEMENT_3D('',#16587,#13721,#13722);
#12118=AXIS2_PLACEMENT_3D('',#16589,#13724,#13725);
#12119=AXIS2_PLACEMENT_3D('',#16590,#13726,#13727);
#12120=AXIS2_PLACEMENT_3D('',#16599,#13732,#13733);
#12121=AXIS2_PLACEMENT_3D('',#16605,#13737,#13738);
#12122=AXIS2_PLACEMENT_3D('',#16611,#13742,#13743);
#12123=AXIS2_PLACEMENT_3D('',#16617,#13747,#13748);
#12124=AXIS2_PLACEMENT_3D('',#16623,#13752,#13753);
#12125=AXIS2_PLACEMENT_3D('',#16626,#13756,#13757);
#12126=AXIS2_PLACEMENT_3D('',#16627,#13758,#13759);
#13684=DIRECTION('axis',(0.,0.,1.));
#13685=DIRECTION('refdir',(1.,0.,0.));
#13686=DIRECTION('center_axis',(0.,1.,0.));
#13687=DIRECTION('ref_axis',(0.,0.,1.));
#13688=DIRECTION('center_axis',(0.,-1.,0.));
#13689=DIRECTION('ref_axis',(1.,0.,0.));
#13690=DIRECTION('center_axis',(0.,-1.,0.));
#13691=DIRECTION('ref_axis',(1.,0.,0.));
#13692=DIRECTION('center_axis',(0.,-1.,0.));
#13693=DIRECTION('ref_axis',(1.,0.,0.));
#13694=DIRECTION('',(0.707106781186548,0.707106781186547,8.65956056235493E-17));
#13695=DIRECTION('center_axis',(0.,-1.,0.));
#13696=DIRECTION('ref_axis',(1.,0.,0.));
#13697=DIRECTION('center_axis',(0.,-1.,0.));
#13698=DIRECTION('ref_axis',(1.,0.,0.));
#13699=DIRECTION('',(0.,1.,0.));
#13700=DIRECTION('center_axis',(0.,1.,0.));
#13701=DIRECTION('ref_axis',(1.,0.,0.));
#13702=DIRECTION('center_axis',(0.,-1.,0.));
#13703=DIRECTION('ref_axis',(1.,0.,0.));
#13704=DIRECTION('',(-0.707106781186547,0.707106781186548,-8.65956056235493E-17));
#13705=DIRECTION('center_axis',(0.,-1.,0.));
#13706=DIRECTION('ref_axis',(0.,0.,-1.));
#13707=DIRECTION('center_axis',(0.,-1.,0.));
#13708=DIRECTION('ref_axis',(1.,0.,0.));
#13709=DIRECTION('center_axis',(0.,1.,0.));
#13710=DIRECTION('ref_axis',(1.,0.,0.));
#13711=DIRECTION('center_axis',(0.,1.,0.));
#13712=DIRECTION('ref_axis',(1.,0.,0.));
#13713=DIRECTION('',(-0.447213595499958,0.894427190999916,-5.47678698264203E-17));
#13714=DIRECTION('center_axis',(0.,-1.,0.));
#13715=DIRECTION('ref_axis',(1.,0.,0.));
#13716=DIRECTION('center_axis',(0.,1.,0.));
#13717=DIRECTION('ref_axis',(1.,0.,0.));
#13718=DIRECTION('',(0.,1.,0.));
#13719=DIRECTION('center_axis',(0.,1.,0.));
#13720=DIRECTION('ref_axis',(1.,0.,0.));
#13721=DIRECTION('center_axis',(0.,-1.,0.));
#13722=DIRECTION('ref_axis',(1.,0.,0.));
#13723=DIRECTION('',(-0.707106781186547,0.707106781186548,-8.65956056235493E-17));
#13724=DIRECTION('center_axis',(0.,-1.,0.));
#13725=DIRECTION('ref_axis',(0.,0.,-1.));
#13726=DIRECTION('center_axis',(0.866025403784439,0.,-0.5));
#13727=DIRECTION('ref_axis',(0.5,0.,0.866025403784439));
#13728=DIRECTION('',(-0.5,0.,-0.866025403784439));
#13729=DIRECTION('',(0.,-1.,0.));
#13730=DIRECTION('',(0.5,0.,0.866025403784439));
#13731=DIRECTION('',(0.,-1.,0.));
#13732=DIRECTION('center_axis',(1.20185167898973E-16,0.,-1.));
#13733=DIRECTION('ref_axis',(1.,0.,1.20185167898973E-16));
#13734=DIRECTION('',(-1.,0.,-1.20185167898973E-16));
#13735=DIRECTION('',(0.,-1.,0.));
#13736=DIRECTION('',(1.,0.,1.20185167898973E-16));
#13737=DIRECTION('center_axis',(-0.866025403784439,0.,-0.5));
#13738=DIRECTION('ref_axis',(0.5,0.,-0.866025403784439));
#13739=DIRECTION('',(-0.5,0.,0.866025403784439));
#13740=DIRECTION('',(0.,-1.,0.));
#13741=DIRECTION('',(0.5,0.,-0.866025403784439));
#13742=DIRECTION('center_axis',(-0.866025403784439,0.,0.5));
#13743=DIRECTION('ref_axis',(-0.5,0.,-0.866025403784439));
#13744=DIRECTION('',(0.5,0.,0.866025403784439));
#13745=DIRECTION('',(0.,-1.,0.));
#13746=DIRECTION('',(-0.5,0.,-0.866025403784439));
#13747=DIRECTION('center_axis',(-2.40370335797945E-16,0.,1.));
#13748=DIRECTION('ref_axis',(-1.,0.,-2.40370335797945E-16));
#13749=DIRECTION('',(1.,0.,2.40370335797945E-16));
#13750=DIRECTION('',(0.,-1.,0.));
#13751=DIRECTION('',(-1.,0.,-2.40370335797945E-16));
#13752=DIRECTION('center_axis',(0.866025403784439,0.,0.5));
#13753=DIRECTION('ref_axis',(-0.5,0.,0.866025403784439));
#13754=DIRECTION('',(0.5,0.,-0.866025403784439));
#13755=DIRECTION('',(-0.5,0.,0.866025403784439));
#13756=DIRECTION('center_axis',(0.,1.,0.));
#13757=DIRECTION('ref_axis',(1.,0.,0.));
#13758=DIRECTION('center_axis',(0.,-1.,0.));
#13759=DIRECTION('ref_axis',(0.,0.,-1.));
#16558=CARTESIAN_POINT('',(0.,0.,0.));
#16559=CARTESIAN_POINT('Origin',(0.375,0.5,0.));
#16560=CARTESIAN_POINT('',(-0.375,0.5,-4.59242549680257E-17));
#16561=CARTESIAN_POINT('Origin',(0.,0.5,0.));
#16562=CARTESIAN_POINT('Origin',(0.,0.475,0.));
#16563=CARTESIAN_POINT('',(-0.425,0.45,-5.20474889637625E-17));
#16564=CARTESIAN_POINT('Origin',(0.,0.45,0.));
#16565=CARTESIAN_POINT('',(-0.4,0.475,-4.89858719658941E-17));
#16566=CARTESIAN_POINT('Origin',(0.,0.24,0.));
#16567=CARTESIAN_POINT('',(-0.425,0.0299999999999998,-5.20474889637625E-17));
#16568=CARTESIAN_POINT('Origin',(0.,0.0299999999999998,0.));
#16569=CARTESIAN_POINT('',(-0.425,0.24,-5.20474889637625E-17));
#16570=CARTESIAN_POINT('Origin',(0.,0.0150000000000001,0.));
#16571=CARTESIAN_POINT('',(-0.395,4.85722573273506E-17,-4.83735485663204E-17));
#16572=CARTESIAN_POINT('Origin',(0.,0.,0.));
#16573=CARTESIAN_POINT('',(-0.41,0.0150000000000001,-5.02105187650415E-17));
#16574=CARTESIAN_POINT('Origin',(0.27,0.,0.));
#16575=CARTESIAN_POINT('',(-0.27,0.,-3.30654635769785E-17));
#16576=CARTESIAN_POINT('Origin',(0.,0.,0.));
#16577=CARTESIAN_POINT('Origin',(0.,-0.02,0.));
#16578=CARTESIAN_POINT('',(-0.24505,-0.0498999999999999,3.00099698131059E-17));
#16579=CARTESIAN_POINT('Origin',(0.,-0.0498999999999999,0.));
#16580=CARTESIAN_POINT('',(-0.26,-0.02,-3.18408167778312E-17));
#16581=CARTESIAN_POINT('Origin',(0.,-0.995,0.));
#16582=CARTESIAN_POINT('',(-0.24505,-1.95495,3.00099698131059E-17));
#16583=CARTESIAN_POINT('Origin',(0.,-1.95495,0.));
#16584=CARTESIAN_POINT('',(-0.24505,-0.995,-3.00099698131059E-17));
#16585=CARTESIAN_POINT('Origin',(0.,-1.975,0.));
#16586=CARTESIAN_POINT('',(-0.2,-2.,-2.44929359829471E-17));
#16587=CARTESIAN_POINT('Origin',(0.,-2.,0.));
#16588=CARTESIAN_POINT('',(-0.225,-1.975,-2.75545529808154E-17));
#16589=CARTESIAN_POINT('Origin',(0.,-2.,0.));
#16590=CARTESIAN_POINT('Origin',(0.115470053837925,-0.5,-0.2));
#16591=CARTESIAN_POINT('',(0.23094010767585,-0.5,0.));
#16592=CARTESIAN_POINT('',(0.115470053837925,-0.5,-0.2));
#16593=CARTESIAN_POINT('',(0.23094010767585,-0.5,0.));
#16594=CARTESIAN_POINT('',(0.115470053837925,-0.8,-0.2));
#16595=CARTESIAN_POINT('',(0.115470053837925,-0.5,-0.2));
#16596=CARTESIAN_POINT('',(0.23094010767585,-0.8,0.));
#16597=CARTESIAN_POINT('',(0.23094010767585,-0.8,0.));
#16598=CARTESIAN_POINT('',(0.23094010767585,-0.5,0.));
#16599=CARTESIAN_POINT('Origin',(-0.115470053837925,-0.5,-0.2));
#16600=CARTESIAN_POINT('',(-0.115470053837925,-0.5,-0.2));
#16601=CARTESIAN_POINT('',(0.115470053837925,-0.5,-0.2));
#16602=CARTESIAN_POINT('',(-0.115470053837925,-0.8,-0.2));
#16603=CARTESIAN_POINT('',(-0.115470053837925,-0.5,-0.2));
#16604=CARTESIAN_POINT('',(0.115470053837925,-0.8,-0.2));
#16605=CARTESIAN_POINT('Origin',(-0.23094010767585,-0.5,-2.77555756156289E-17));
#16606=CARTESIAN_POINT('',(-0.23094010767585,-0.5,-2.82820063659975E-17));
#16607=CARTESIAN_POINT('',(-0.115470053837925,-0.5,-0.2));
#16608=CARTESIAN_POINT('',(-0.23094010767585,-0.8,-2.77555756156289E-17));
#16609=CARTESIAN_POINT('',(-0.23094010767585,-0.5,-2.82820063659975E-17));
#16610=CARTESIAN_POINT('',(-0.115470053837925,-0.8,-0.2));
#16611=CARTESIAN_POINT('Origin',(-0.115470053837925,-0.5,0.2));
#16612=CARTESIAN_POINT('',(-0.115470053837925,-0.5,0.2));
#16613=CARTESIAN_POINT('',(-0.23094010767585,-0.5,-2.82820063659975E-17));
#16614=CARTESIAN_POINT('',(-0.115470053837925,-0.8,0.2));
#16615=CARTESIAN_POINT('',(-0.115470053837925,-0.5,0.2));
#16616=CARTESIAN_POINT('',(-0.23094010767585,-0.8,-2.82820063659975E-17));
#16617=CARTESIAN_POINT('Origin',(0.115470053837925,-0.5,0.2));
#16618=CARTESIAN_POINT('',(0.115470053837925,-0.5,0.2));
#16619=CARTESIAN_POINT('',(-0.115470053837925,-0.5,0.2));
#16620=CARTESIAN_POINT('',(0.115470053837925,-0.8,0.2));
#16621=CARTESIAN_POINT('',(0.115470053837925,-0.5,0.2));
#16622=CARTESIAN_POINT('',(-0.115470053837925,-0.8,0.2));
#16623=CARTESIAN_POINT('Origin',(0.23094010767585,-0.5,0.));
#16624=CARTESIAN_POINT('',(0.115470053837925,-0.5,0.2));
#16625=CARTESIAN_POINT('',(0.115470053837925,-0.8,0.2));
#16626=CARTESIAN_POINT('Origin',(0.,-0.5,0.));
#16627=CARTESIAN_POINT('Origin',(0.,-0.8,0.));
#53823=UNCERTAINTY_MEASURE_WITH_UNIT(LENGTH_MEASURE(0.001),#53910,
'DISTANCE_ACCURACY_VALUE',
'Maximum model space distance between geometric entities at asserted c
onnectivities');
#53859=UNCERTAINTY_MEASURE_WITH_UNIT(LENGTH_MEASURE(0.001),#53910,
'DISTANCE_ACCURACY_VALUE',
'Maximum model space distance between geometric entities at asserted c
onnectivities');
#53873=(
GEOMETRIC_REPRESENTATION_CONTEXT(3)
GLOBAL_UNCERTAINTY_ASSIGNED_CONTEXT((#53823))
GLOBAL_UNIT_ASSIGNED_CONTEXT((#53910,#53912,#53913))
REPRESENTATION_CONTEXT('','3D')
);
#53909=(
GEOMETRIC_REPRESENTATION_CONTEXT(3)
GLOBAL_UNCERTAINTY_ASSIGNED_CONTEXT((#53859))
GLOBAL_UNIT_ASSIGNED_CONTEXT((#53910,#53912,#53913))
REPRESENTATION_CONTEXT('','3D')
);
#53910=(
LENGTH_UNIT()
NAMED_UNIT(*)
SI_UNIT(.CENTI.,.METRE.)
);
#53912=(
NAMED_UNIT(*)
PLANE_ANGLE_UNIT()
SI_UNIT($,.RADIAN.)
);
#53913=(
NAMED_UNIT(*)
SI_UNIT($,.STERADIAN.)
SOLID_ANGLE_UNIT()
);
#53927=SHAPE_DEFINITION_REPRESENTATION(#53976,#54099);
#53976=PRODUCT_DEFINITION_SHAPE('',$,#54149);
#54099=SHAPE_REPRESENTATION('',(#12101),#53873);
#54135=PRODUCT_DEFINITION_CONTEXT('part definition',#54284,'design');
#54149=PRODUCT_DEFINITION('Cap Screw - M5x20','Cap Screw - M5x20',#54198,
#54135);
#54198=PRODUCT_DEFINITION_FORMATION('',$,#54299);
#54284=APPLICATION_CONTEXT(
'Core Data for Automotive Mechanical Design Process');
#54285=PRODUCT_CONTEXT('part definition',#54284,'mechanical');
#54299=PRODUCT('Cap Screw - M5x20','Cap Screw - M5x20',
'Cap Screw - M5x20',(#54285));
#54398=COLOUR_RGB('Black',0.12,0.14,0.17);
#54399=FILL_AREA_STYLE_COLOUR('',#54398);
#54400=FILL_AREA_STYLE('',(#54399));
#54401=SURFACE_STYLE_FILL_AREA(#54400);
#54402=SURFACE_SIDE_STYLE('',(#54401));
#54403=SURFACE_STYLE_USAGE(.BOTH.,#54402);
#54404=PRESENTATION_STYLE_ASSIGNMENT((#54403));
ENDSEC;
END-ISO-10303-21;
